ISO-10303-21;
HEADER;
/* Generated by software containing ST-Developer
 * from STEP Tools, Inc. (www.steptools.com) 
 */

FILE_DESCRIPTION(
/* description */ ('Double-bearing flanged cartridge'),
/* implementation_level */ '2;1');

FILE_NAME(
/* name */ 'Cap Screw - M4x16.step',
/* time_stamp */ '2026-10-28T03:26:40-07:00',
/* author */ (''),
/* organization */ (''),
/* preprocessor_version */ 'ST-DEVELOPER v20.2',
/* originating_system */ 'Autodesk Translation Framework v15.17.0.0',
/* authorisation */ '');

FILE_SCHEMA (('AUTOMOTIVE_DESIGN { 1 0 10303 214 3 1 1 }'));
ENDSEC;

DATA;
#10=MECHANICAL_DESIGN_GEOMETRIC_PRESENTATION_REPRESENTATION('',(#208),#5535);
#14=ORIENTED_CLOSED_SHELL('',*,#2343,.F.);
#15=BREP_WITH_VOIDS('Body1',#2342,(#14));
#156=CONICAL_SURFACE('',#2774,0.325,0.785398163397448);
#157=CONICAL_SURFACE('',#2778,0.335,0.785398163397448);
#158=CONICAL_SURFACE('',#2782,0.21,0.463647609000806);
#159=CONICAL_SURFACE('',#2786,0.18,0.785398163397448);
#172=SHAPE_REPRESENTATION_RELATIONSHIP('SRR','None',#5614,#186);
#186=ADVANCED_BREP_SHAPE_REPRESENTATION('',(#15),#5530);
#208=STYLED_ITEM('',(#5771),#15);
#289=FACE_BOUND('',#680,.T.);
#340=PLANE('',#2772);
#341=PLANE('',#2780);
#342=PLANE('',#2788);
#343=PLANE('',#2789);
#344=PLANE('',#2790);
#345=PLANE('',#2791);
#346=PLANE('',#2792);
#347=PLANE('',#2793);
#348=PLANE('',#2794);
#349=PLANE('',#2795);
#350=PLANE('',#2796);
#470=FACE_OUTER_BOUND('',#675,.T.);
#471=FACE_OUTER_BOUND('',#676,.T.);
#472=FACE_OUTER_BOUND('',#677,.T.);
#473=FACE_OUTER_BOUND('',#678,.T.);
#474=FACE_OUTER_BOUND('',#679,.T.);
#475=FACE_OUTER_BOUND('',#681,.T.);
#476=FACE_OUTER_BOUND('',#682,.T.);
#477=FACE_OUTER_BOUND('',#683,.T.);
#478=FACE_OUTER_BOUND('',#684,.T.);
#479=FACE_OUTER_BOUND('',#685,.T.);
#480=FACE_OUTER_BOUND('',#686,.T.);
#481=FACE_OUTER_BOUND('',#687,.T.);
#482=FACE_OUTER_BOUND('',#688,.T.);
#483=FACE_OUTER_BOUND('',#689,.T.);
#484=FACE_OUTER_BOUND('',#690,.T.);
#485=FACE_OUTER_BOUND('',#691,.T.);
#486=FACE_OUTER_BOUND('',#692,.T.);
#675=EDGE_LOOP('',(#1972));
#676=EDGE_LOOP('',(#1973,#1974,#1975,#1976));
#677=EDGE_LOOP('',(#1977,#1978,#1979,#1980));
#678=EDGE_LOOP('',(#1981,#1982,#1983,#1984));
#679=EDGE_LOOP('',(#1985));
#680=EDGE_LOOP('',(#1986));
#681=EDGE_LOOP('',(#1987,#1988,#1989,#1990));
#682=EDGE_LOOP('',(#1991,#1992,#1993,#1994));
#683=EDGE_LOOP('',(#1995,#1996,#1997,#1998));
#684=EDGE_LOOP('',(#1999));
#685=EDGE_LOOP('',(#2000,#2001,#2002,#2003));
#686=EDGE_LOOP('',(#2004,#2005,#2006,#2007));
#687=EDGE_LOOP('',(#2008,#2009,#2010,#2011));
#688=EDGE_LOOP('',(#2012,#2013,#2014,#2015));
#689=EDGE_LOOP('',(#2016,#2017,#2018,#2019));
#690=EDGE_LOOP('',(#2020,#2021,#2022,#2023));
#691=EDGE_LOOP('',(#2024,#2025,#2026,#2027,#2028,#2029));
#692=EDGE_LOOP('',(#2030,#2031,#2032,#2033,#2034,#2035));
#777=LINE('',#4516,#863);
#778=LINE('',#4520,#864);
#779=LINE('',#4524,#865);
#780=LINE('',#4531,#866);
#781=LINE('',#4535,#867);
#782=LINE('',#4539,#868);
#783=LINE('',#4544,#869);
#784=LINE('',#4546,#870);
#785=LINE('',#4548,#871);
#786=LINE('',#4549,#872);
#787=LINE('',#4552,#873);
#788=LINE('',#4554,#874);
#789=LINE('',#4555,#875);
#790=LINE('',#4558,#876);
#791=LINE('',#4560,#877);
#792=LINE('',#4561,#878);
#793=LINE('',#4564,#879);
#794=LINE('',#4566,#880);
#795=LINE('',#4567,#881);
#796=LINE('',#4570,#882);
#797=LINE('',#4572,#883);
#798=LINE('',#4573,#884);
#799=LINE('',#4575,#885);
#800=LINE('',#4576,#886);
#863=VECTOR('',#3466,0.325);
#864=VECTOR('',#3471,0.35);
#865=VECTOR('',#3476,0.335);
#866=VECTOR('',#3485,0.21);
#867=VECTOR('',#3490,0.2);
#868=VECTOR('',#3495,0.18);
#869=VECTOR('',#3500,1.);
#870=VECTOR('',#3501,1.);
#871=VECTOR('',#3502,1.);
#872=VECTOR('',#3503,1.);
#873=VECTOR('',#3506,1.);
#874=VECTOR('',#3507,1.);
#875=VECTOR('',#3508,1.);
#876=VECTOR('',#3511,1.);
#877=VECTOR('',#3512,1.);
#878=VECTOR('',#3513,1.);
#879=VECTOR('',#3516,1.);
#880=VECTOR('',#3517,1.);
#881=VECTOR('',#3518,1.);
#882=VECTOR('',#3521,1.);
#883=VECTOR('',#3522,1.);
#884=VECTOR('',#3523,1.);
#885=VECTOR('',#3526,1.);
#886=VECTOR('',#3527,1.);
#1040=CIRCLE('',#2773,0.3);
#1041=CIRCLE('',#2775,0.35);
#1042=CIRCLE('',#2777,0.35);
#1043=CIRCLE('',#2779,0.32);
#1044=CIRCLE('',#2781,0.22);
#1045=CIRCLE('',#2783,0.1954);
#1046=CIRCLE('',#2785,0.1954);
#1047=CIRCLE('',#2787,0.16);
#1222=VERTEX_POINT('',#4511);
#1223=VERTEX_POINT('',#4514);
#1224=VERTEX_POINT('',#4518);
#1225=VERTEX_POINT('',#4522);
#1226=VERTEX_POINT('',#4526);
#1227=VERTEX_POINT('',#4529);
#1228=VERTEX_POINT('',#4533);
#1229=VERTEX_POINT('',#4537);
#1230=VERTEX_POINT('',#4542);
#1231=VERTEX_POINT('',#4543);
#1232=VERTEX_POINT('',#4545);
#1233=VERTEX_POINT('',#4547);
#1234=VERTEX_POINT('',#4551);
#1235=VERTEX_POINT('',#4553);
#1236=VERTEX_POINT('',#4557);
#1237=VERTEX_POINT('',#4559);
#1238=VERTEX_POINT('',#4563);
#1239=VERTEX_POINT('',#4565);
#1240=VERTEX_POINT('',#4569);
#1241=VERTEX_POINT('',#4571);
#1479=EDGE_CURVE('',#1222,#1222,#1040,.T.);
#1480=EDGE_CURVE('',#1223,#1223,#1041,.T.);
#1481=EDGE_CURVE('',#1223,#1222,#777,.T.);
#1482=EDGE_CURVE('',#1224,#1224,#1042,.T.);
#1483=EDGE_CURVE('',#1224,#1223,#778,.T.);
#1484=EDGE_CURVE('',#1225,#1225,#1043,.T.);
#1485=EDGE_CURVE('',#1225,#1224,#779,.T.);
#1486=EDGE_CURVE('',#1226,#1226,#1044,.T.);
#1487=EDGE_CURVE('',#1227,#1227,#1045,.F.);
#1488=EDGE_CURVE('',#1227,#1226,#780,.T.);
#1489=EDGE_CURVE('',#1228,#1228,#1046,.F.);
#1490=EDGE_CURVE('',#1228,#1227,#781,.T.);
#1491=EDGE_CURVE('',#1229,#1229,#1047,.T.);
#1492=EDGE_CURVE('',#1229,#1228,#782,.T.);
#1493=EDGE_CURVE('',#1230,#1231,#783,.T.);
#1494=EDGE_CURVE('',#1231,#1232,#784,.T.);
#1495=EDGE_CURVE('',#1232,#1233,#785,.T.);
#1496=EDGE_CURVE('',#1230,#1233,#786,.T.);
#1497=EDGE_CURVE('',#1231,#1234,#787,.T.);
#1498=EDGE_CURVE('',#1234,#1235,#788,.T.);
#1499=EDGE_CURVE('',#1235,#1232,#789,.T.);
#1500=EDGE_CURVE('',#1234,#1236,#790,.T.);
#1501=EDGE_CURVE('',#1236,#1237,#791,.T.);
#1502=EDGE_CURVE('',#1237,#1235,#792,.T.);
#1503=EDGE_CURVE('',#1236,#1238,#793,.T.);
#1504=EDGE_CURVE('',#1238,#1239,#794,.T.);
#1505=EDGE_CURVE('',#1239,#1237,#795,.T.);
#1506=EDGE_CURVE('',#1238,#1240,#796,.T.);
#1507=EDGE_CURVE('',#1240,#1241,#797,.T.);
#1508=EDGE_CURVE('',#1241,#1239,#798,.T.);
#1509=EDGE_CURVE('',#1240,#1230,#799,.T.);
#1510=EDGE_CURVE('',#1233,#1241,#800,.T.);
#1972=ORIENTED_EDGE('',*,*,#1479,.F.);
#1973=ORIENTED_EDGE('',*,*,#1480,.F.);
#1974=ORIENTED_EDGE('',*,*,#1481,.T.);
#1975=ORIENTED_EDGE('',*,*,#1479,.T.);
#1976=ORIENTED_EDGE('',*,*,#1481,.F.);
#1977=ORIENTED_EDGE('',*,*,#1482,.F.);
#1978=ORIENTED_EDGE('',*,*,#1483,.T.);
#1979=ORIENTED_EDGE('',*,*,#1480,.T.);
#1980=ORIENTED_EDGE('',*,*,#1483,.F.);
#1981=ORIENTED_EDGE('',*,*,#1484,.F.);
#1982=ORIENTED_EDGE('',*,*,#1485,.T.);
#1983=ORIENTED_EDGE('',*,*,#1482,.T.);
#1984=ORIENTED_EDGE('',*,*,#1485,.F.);
#1985=ORIENTED_EDGE('',*,*,#1484,.T.);
#1986=ORIENTED_EDGE('',*,*,#1486,.F.);
#1987=ORIENTED_EDGE('',*,*,#1487,.F.);
#1988=ORIENTED_EDGE('',*,*,#1488,.T.);
#1989=ORIENTED_EDGE('',*,*,#1486,.T.);
#1990=ORIENTED_EDGE('',*,*,#1488,.F.);
#1991=ORIENTED_EDGE('',*,*,#1489,.F.);
#1992=ORIENTED_EDGE('',*,*,#1490,.T.);
#1993=ORIENTED_EDGE('',*,*,#1487,.T.);
#1994=ORIENTED_EDGE('',*,*,#1490,.F.);
#1995=ORIENTED_EDGE('',*,*,#1491,.F.);
#1996=ORIENTED_EDGE('',*,*,#1492,.T.);
#1997=ORIENTED_EDGE('',*,*,#1489,.T.);
#1998=ORIENTED_EDGE('',*,*,#1492,.F.);
#1999=ORIENTED_EDGE('',*,*,#1491,.T.);
#2000=ORIENTED_EDGE('',*,*,#1493,.T.);
#2001=ORIENTED_EDGE('',*,*,#1494,.T.);
#2002=ORIENTED_EDGE('',*,*,#1495,.T.);
#2003=ORIENTED_EDGE('',*,*,#1496,.F.);
#2004=ORIENTED_EDGE('',*,*,#1497,.T.);
#2005=ORIENTED_EDGE('',*,*,#1498,.T.);
#2006=ORIENTED_EDGE('',*,*,#1499,.T.);
#2007=ORIENTED_EDGE('',*,*,#1494,.F.);
#2008=ORIENTED_EDGE('',*,*,#1500,.T.);
#2009=ORIENTED_EDGE('',*,*,#1501,.T.);
#2010=ORIENTED_EDGE('',*,*,#1502,.T.);
#2011=ORIENTED_EDGE('',*,*,#1498,.F.);
#2012=ORIENTED_EDGE('',*,*,#1503,.T.);
#2013=ORIENTED_EDGE('',*,*,#1504,.T.);
#2014=ORIENTED_EDGE('',*,*,#1505,.T.);
#2015=ORIENTED_EDGE('',*,*,#1501,.F.);
#2016=ORIENTED_EDGE('',*,*,#1506,.T.);
#2017=ORIENTED_EDGE('',*,*,#1507,.T.);
#2018=ORIENTED_EDGE('',*,*,#1508,.T.);
#2019=ORIENTED_EDGE('',*,*,#1504,.F.);
#2020=ORIENTED_EDGE('',*,*,#1509,.T.);
#2021=ORIENTED_EDGE('',*,*,#1496,.T.);
#2022=ORIENTED_EDGE('',*,*,#1510,.T.);
#2023=ORIENTED_EDGE('',*,*,#1507,.F.);
#2024=ORIENTED_EDGE('',*,*,#1509,.F.);
#2025=ORIENTED_EDGE('',*,*,#1506,.F.);
#2026=ORIENTED_EDGE('',*,*,#1503,.F.);
#2027=ORIENTED_EDGE('',*,*,#1500,.F.);
#2028=ORIENTED_EDGE('',*,*,#1497,.F.);
#2029=ORIENTED_EDGE('',*,*,#1493,.F.);
#2030=ORIENTED_EDGE('',*,*,#1510,.F.);
#2031=ORIENTED_EDGE('',*,*,#1495,.F.);
#2032=ORIENTED_EDGE('',*,*,#1499,.F.);
#2033=ORIENTED_EDGE('',*,*,#1502,.F.);
#2034=ORIENTED_EDGE('',*,*,#1505,.F.);
#2035=ORIENTED_EDGE('',*,*,#1508,.F.);
#2161=CYLINDRICAL_SURFACE('',#2776,0.35);
#2162=CYLINDRICAL_SURFACE('',#2784,0.1954);
#2284=ADVANCED_FACE('',(#470),#340,.T.);
#2285=ADVANCED_FACE('',(#471),#156,.T.);
#2286=ADVANCED_FACE('',(#472),#2161,.T.);
#2287=ADVANCED_FACE('',(#473),#157,.T.);
#2288=ADVANCED_FACE('',(#474,#289),#341,.T.);
#2289=ADVANCED_FACE('',(#475),#158,.T.);
#2290=ADVANCED_FACE('',(#476),#2162,.T.);
#2291=ADVANCED_FACE('',(#477),#159,.T.);
#2292=ADVANCED_FACE('',(#478),#342,.T.);
#2293=ADVANCED_FACE('',(#479),#343,.F.);
#2294=ADVANCED_FACE('',(#480),#344,.F.);
#2295=ADVANCED_FACE('',(#481),#345,.F.);
#2296=ADVANCED_FACE('',(#482),#346,.F.);
#2297=ADVANCED_FACE('',(#483),#347,.F.);
#2298=ADVANCED_FACE('',(#484),#348,.F.);
#2299=ADVANCED_FACE('',(#485),#349,.F.);
#2300=ADVANCED_FACE('',(#486),#350,.F.);
#2342=CLOSED_SHELL('',(#2284,#2285,#2286,#2287,#2288,#2289,#2290,#2291,
#2292));
#2343=CLOSED_SHELL('',(#2293,#2294,#2295,#2296,#2297,#2298,#2299,#2300));
#2771=AXIS2_PLACEMENT_3D('',#4509,#3456,#3457);
#2772=AXIS2_PLACEMENT_3D('',#4510,#3458,#3459);
#2773=AXIS2_PLACEMENT_3D('',#4512,#3460,#3461);
#2774=AXIS2_PLACEMENT_3D('',#4513,#3462,#3463);
#2775=AXIS2_PLACEMENT_3D('',#4515,#3464,#3465);
#2776=AXIS2_PLACEMENT_3D('',#4517,#3467,#3468);
#2777=AXIS2_PLACEMENT_3D('',#4519,#3469,#3470);
#2778=AXIS2_PLACEMENT_3D('',#4521,#3472,#3473);
#2779=AXIS2_PLACEMENT_3D('',#4523,#3474,#3475);
#2780=AXIS2_PLACEMENT_3D('',#4525,#3477,#3478);
#2781=AXIS2_PLACEMENT_3D('',#4527,#3479,#3480);
#2782=AXIS2_PLACEMENT_3D('',#4528,#3481,#3482);
#2783=AXIS2_PLACEMENT_3D('',#4530,#3483,#3484);
#2784=AXIS2_PLACEMENT_3D('',#4532,#3486,#3487);
#2785=AXIS2_PLACEMENT_3D('',#4534,#3488,#3489);
#2786=AXIS2_PLACEMENT_3D('',#4536,#3491,#3492);
#2787=AXIS2_PLACEMENT_3D('',#4538,#3493,#3494);
#2788=AXIS2_PLACEMENT_3D('',#4540,#3496,#3497);
#2789=AXIS2_PLACEMENT_3D('',#4541,#3498,#3499);
#2790=AXIS2_PLACEMENT_3D('',#4550,#3504,#3505);
#2791=AXIS2_PLACEMENT_3D('',#4556,#3509,#3510);
#2792=AXIS2_PLACEMENT_3D('',#4562,#3514,#3515);
#2793=AXIS2_PLACEMENT_3D('',#4568,#3519,#3520);
#2794=AXIS2_PLACEMENT_3D('',#4574,#3524,#3525);
#2795=AXIS2_PLACEMENT_3D('',#4577,#3528,#3529);
#2796=AXIS2_PLACEMENT_3D('',#4578,#3530,#3531);
#3456=DIRECTION('axis',(0.,0.,1.));
#3457=DIRECTION('refdir',(1.,0.,0.));
#3458=DIRECTION('center_axis',(0.,1.,0.));
#3459=DIRECTION('ref_axis',(0.,0.,1.));
#3460=DIRECTION('center_axis',(0.,-1.,0.));
#3461=DIRECTION('ref_axis',(1.,0.,0.));
#3462=DIRECTION('center_axis',(0.,-1.,0.));
#3463=DIRECTION('ref_axis',(1.,0.,0.));
#3464=DIRECTION('center_axis',(0.,-1.,0.));
#3465=DIRECTION('ref_axis',(1.,0.,0.));
#3466=DIRECTION('',(0.707106781186547,0.707106781186548,8.65956056235493E-17));
#3467=DIRECTION('center_axis',(0.,-1.,0.));
#3468=DIRECTION('ref_axis',(1.,0.,0.));
#3469=DIRECTION('center_axis',(0.,-1.,0.));
#3470=DIRECTION('ref_axis',(1.,0.,0.));
#3471=DIRECTION('',(0.,1.,0.));
#3472=DIRECTION('center_axis',(0.,1.,0.));
#3473=DIRECTION('ref_axis',(1.,0.,0.));
#3474=DIRECTION('center_axis',(0.,-1.,0.));
#3475=DIRECTION('ref_axis',(1.,0.,0.));
#3476=DIRECTION('',(-0.707106781186547,0.707106781186548,-8.65956056235493E-17));
#3477=DIRECTION('center_axis',(0.,-1.,0.));
#3478=DIRECTION('ref_axis',(0.,0.,-1.));
#3479=DIRECTION('center_axis',(0.,-1.,0.));
#3480=DIRECTION('ref_axis',(1.,0.,0.));
#3481=DIRECTION('center_axis',(0.,1.,0.));
#3482=DIRECTION('ref_axis',(1.,0.,0.));
#3483=DIRECTION('center_axis',(0.,1.,0.));
#3484=DIRECTION('ref_axis',(1.,0.,0.));
#3485=DIRECTION('',(-0.447213595499958,0.894427190999916,-5.47678698264203E-17));
#3486=DIRECTION('center_axis',(0.,-1.,0.));
#3487=DIRECTION('ref_axis',(1.,0.,0.));
#3488=DIRECTION('center_axis',(0.,1.,0.));
#3489=DIRECTION('ref_axis',(1.,0.,0.));
#3490=DIRECTION('',(0.,1.,0.));
#3491=DIRECTION('center_axis',(0.,1.,0.));
#3492=DIRECTION('ref_axis',(1.,0.,0.));
#3493=DIRECTION('center_axis',(0.,-1.,0.));
#3494=DIRECTION('ref_axis',(1.,0.,0.));
#3495=DIRECTION('',(-0.707106781186547,0.707106781186548,-8.65956056235493E-17));
#3496=DIRECTION('center_axis',(0.,-1.,0.));
#3497=DIRECTION('ref_axis',(0.,0.,-1.));
#3498=DIRECTION('center_axis',(0.866025403784439,0.,-0.5));
#3499=DIRECTION('ref_axis',(0.5,0.,0.866025403784439));
#3500=DIRECTION('',(-0.5,0.,-0.866025403784439));
#3501=DIRECTION('',(0.,-1.,0.));
#3502=DIRECTION('',(0.5,0.,0.866025403784439));
#3503=DIRECTION('',(0.,-1.,0.));
#3504=DIRECTION('center_axis',(1.60246890531964E-16,0.,-1.));
#3505=DIRECTION('ref_axis',(1.,0.,1.60246890531964E-16));
#3506=DIRECTION('',(-1.,0.,-1.60246890531964E-16));
#3507=DIRECTION('',(0.,-1.,0.));
#3508=DIRECTION('',(1.,0.,1.60246890531964E-16));
#3509=DIRECTION('center_axis',(-0.866025403784439,0.,-0.5));
#3510=DIRECTION('ref_axis',(0.5,0.,-0.866025403784439));
#3511=DIRECTION('',(-0.5,0.,0.866025403784439));
#3512=DIRECTION('',(0.,-1.,0.));
#3513=DIRECTION('',(0.5,0.,-0.866025403784439));
#3514=DIRECTION('center_axis',(-0.866025403784439,0.,0.5));
#3515=DIRECTION('ref_axis',(-0.5,0.,-0.866025403784439));
#3516=DIRECTION('',(0.5,0.,0.866025403784439));
#3517=DIRECTION('',(0.,-1.,0.));
#3518=DIRECTION('',(-0.5,0.,-0.866025403784439));
#3519=DIRECTION('center_axis',(-1.60246890531964E-16,0.,1.));
#3520=DIRECTION('ref_axis',(-1.,0.,-1.60246890531964E-16));
#3521=DIRECTION('',(1.,0.,1.60246890531964E-16));
#3522=DIRECTION('',(0.,-1.,0.));
#3523=DIRECTION('',(-1.,0.,-1.60246890531964E-16));
#3524=DIRECTION('center_axis',(0.866025403784439,0.,0.5));
#3525=DIRECTION('ref_axis',(-0.5,0.,0.866025403784439));
#3526=DIRECTION('',(0.5,0.,-0.866025403784439));
#3527=DIRECTION('',(-0.5,0.,0.866025403784439));
#3528=DIRECTION('center_axis',(0.,1.,0.));
#3529=DIRECTION('ref_axis',(1.,0.,0.));
#3530=DIRECTION('center_axis',(0.,-1.,0.));
#3531=DIRECTION('ref_axis',(0.,0.,-1.));
#4509=CARTESIAN_POINT('',(0.,0.,0.));
#4510=CARTESIAN_POINT('Origin',(0.3,0.4,0.));
#4511=CARTESIAN_POINT('',(-0.3,0.4,-3.67394039744206E-17));
#4512=CARTESIAN_POINT('Origin',(0.,0.4,0.));
#4513=CARTESIAN_POINT('Origin',(0.,0.375,0.));
#4514=CARTESIAN_POINT('',(-0.35,0.35,-4.28626379701573E-17));
#4515=CARTESIAN_POINT('Origin',(0.,0.35,0.));
#4516=CARTESIAN_POINT('',(-0.325,0.375,-3.9801020972289E-17));
#4517=CARTESIAN_POINT('Origin',(0.,0.19,0.));
#4518=CARTESIAN_POINT('',(-0.35,0.03,-4.28626379701574E-17));
#4519=CARTESIAN_POINT('Origin',(0.,0.03,0.));
#4520=CARTESIAN_POINT('',(-0.35,0.19,-4.28626379701574E-17));
#4521=CARTESIAN_POINT('Origin',(0.,0.0149999999999999,0.));
#4522=CARTESIAN_POINT('',(-0.32,-3.29597460435593E-17,-3.91886975727153E-17));
#4523=CARTESIAN_POINT('Origin',(0.,0.,0.));
#4524=CARTESIAN_POINT('',(-0.335,0.0149999999999999,-4.10256677714363E-17));
#4525=CARTESIAN_POINT('Origin',(0.22,0.,0.));
#4526=CARTESIAN_POINT('',(-0.22,-6.93889390390723E-18,-2.69422295812418E-17));
#4527=CARTESIAN_POINT('Origin',(0.,0.,0.));
#4528=CARTESIAN_POINT('Origin',(0.,-0.02,0.));
#4529=CARTESIAN_POINT('',(-0.1954,-0.0492,2.39295984553393E-17));
#4530=CARTESIAN_POINT('Origin',(0.,-0.0492,0.));
#4531=CARTESIAN_POINT('',(-0.21,-0.02,-2.57175827820944E-17));
#4532=CARTESIAN_POINT('Origin',(0.,-0.8,0.));
#4533=CARTESIAN_POINT('',(-0.1954,-1.5646,2.39295984553393E-17));
#4534=CARTESIAN_POINT('Origin',(0.,-1.5646,0.));
#4535=CARTESIAN_POINT('',(-0.1954,-0.8,-2.39295984553393E-17));
#4536=CARTESIAN_POINT('Origin',(0.,-1.58,0.));
#4537=CARTESIAN_POINT('',(-0.16,-1.6,-1.95943487863577E-17));
#4538=CARTESIAN_POINT('Origin',(0.,-1.6,0.));
#4539=CARTESIAN_POINT('',(-0.18,-1.58,-2.20436423846524E-17));
#4540=CARTESIAN_POINT('Origin',(0.,-1.6,0.));
#4541=CARTESIAN_POINT('Origin',(0.0866025403784439,-0.4,-0.15));
#4542=CARTESIAN_POINT('',(0.173205080756888,-0.4,0.));
#4543=CARTESIAN_POINT('',(0.0866025403784439,-0.4,-0.15));
#4544=CARTESIAN_POINT('',(0.173205080756888,-0.4,0.));
#4545=CARTESIAN_POINT('',(0.0866025403784439,-0.64,-0.15));
#4546=CARTESIAN_POINT('',(0.0866025403784439,-0.4,-0.15));
#4547=CARTESIAN_POINT('',(0.173205080756888,-0.64,0.));
#4548=CARTESIAN_POINT('',(0.173205080756888,-0.64,0.));
#4549=CARTESIAN_POINT('',(0.173205080756888,-0.4,0.));
#4550=CARTESIAN_POINT('Origin',(-0.0866025403784438,-0.4,-0.15));
#4551=CARTESIAN_POINT('',(-0.0866025403784438,-0.4,-0.15));
#4552=CARTESIAN_POINT('',(0.0866025403784439,-0.4,-0.15));
#4553=CARTESIAN_POINT('',(-0.0866025403784438,-0.64,-0.15));
#4554=CARTESIAN_POINT('',(-0.0866025403784438,-0.4,-0.15));
#4555=CARTESIAN_POINT('',(0.0866025403784439,-0.64,-0.15));
#4556=CARTESIAN_POINT('Origin',(-0.173205080756888,-0.4,-2.77555756156289E-17));
#4557=CARTESIAN_POINT('',(-0.173205080756888,-0.4,-2.12115047744981E-17));
#4558=CARTESIAN_POINT('',(-0.0866025403784438,-0.4,-0.15));
#4559=CARTESIAN_POINT('',(-0.173205080756888,-0.64,-2.77555756156289E-17));
#4560=CARTESIAN_POINT('',(-0.173205080756888,-0.4,-2.12115047744981E-17));
#4561=CARTESIAN_POINT('',(-0.0866025403784438,-0.64,-0.15));
#4562=CARTESIAN_POINT('Origin',(-0.0866025403784439,-0.4,0.15));
#4563=CARTESIAN_POINT('',(-0.0866025403784439,-0.4,0.15));
#4564=CARTESIAN_POINT('',(-0.173205080756888,-0.4,-2.12115047744981E-17));
#4565=CARTESIAN_POINT('',(-0.0866025403784439,-0.64,0.15));
#4566=CARTESIAN_POINT('',(-0.0866025403784439,-0.4,0.15));
#4567=CARTESIAN_POINT('',(-0.173205080756888,-0.64,-2.12115047744981E-17));
#4568=CARTESIAN_POINT('Origin',(0.0866025403784439,-0.4,0.15));
#4569=CARTESIAN_POINT('',(0.0866025403784439,-0.4,0.15));
#4570=CARTESIAN_POINT('',(-0.0866025403784439,-0.4,0.15));
#4571=CARTESIAN_POINT('',(0.0866025403784439,-0.64,0.15));
#4572=CARTESIAN_POINT('',(0.0866025403784439,-0.4,0.15));
#4573=CARTESIAN_POINT('',(-0.0866025403784439,-0.64,0.15));
#4574=CARTESIAN_POINT('Origin',(0.173205080756888,-0.4,0.));
#4575=CARTESIAN_POINT('',(0.0866025403784439,-0.4,0.15));
#4576=CARTESIAN_POINT('',(0.0866025403784439,-0.64,0.15));
#4577=CARTESIAN_POINT('Origin',(0.,-0.4,-2.77555756156289E-17));
#4578=CARTESIAN_POINT('Origin',(0.,-0.64,-2.77555756156289E-17));
#5511=UNCERTAINTY_MEASURE_WITH_UNIT(LENGTH_MEASURE(0.001),#5536,
'DISTANCE_ACCURACY_VALUE',
'Maximum model space distance between geometric entities at asserted c
onnectivities');
#5516=UNCERTAINTY_MEASURE_WITH_UNIT(LENGTH_MEASURE(0.001),#5536,
'DISTANCE_ACCURACY_VALUE',
'Maximum model space distance between geometric entities at asserted c
onnectivities');
#5530=(
GEOMETRIC_REPRESENTATION_CONTEXT(3)
GLOBAL_UNCERTAINTY_ASSIGNED_CONTEXT((#5511))
GLOBAL_UNIT_ASSIGNED_CONTEXT((#5536,#5538,#5539))
REPRESENTATION_CONTEXT('','3D')
);
#5535=(
GEOMETRIC_REPRESENTATION_CONTEXT(3)
GLOBAL_UNCERTAINTY_ASSIGNED_CONTEXT((#5516))
GLOBAL_UNIT_ASSIGNED_CONTEXT((#5536,#5538,#5539))
REPRESENTATION_CONTEXT('','3D')
);
#5536=(
LENGTH_UNIT()
NAMED_UNIT(*)
SI_UNIT(.CENTI.,.METRE.)
);
#5538=(
NAMED_UNIT(*)
PLANE_ANGLE_UNIT()
SI_UNIT($,.RADIAN.)
);
#5539=(
NAMED_UNIT(*)
SI_UNIT($,.STERADIAN.)
SOLID_ANGLE_UNIT()
);
#5553=SHAPE_DEFINITION_REPRESENTATION(#5576,#5614);
#5576=PRODUCT_DEFINITION_SHAPE('',$,#5633);
#5614=SHAPE_REPRESENTATION('',(#2771),#5530);
#5619=PRODUCT_DEFINITION_CONTEXT('part definition',#5675,'design');
#5633=PRODUCT_DEFINITION('Cap Screw - M4x16','Cap Screw - M4x16',#5651,
#5619);
#5651=PRODUCT_DEFINITION_FORMATION('',$,#5690);
#5675=APPLICATION_CONTEXT(
'Core Data for Automotive Mechanical Design Process');
#5676=PRODUCT_CONTEXT('part definition',#5675,'mechanical');
#5690=PRODUCT('Cap Screw - M4x16','Cap Screw - M4x16',
'Cap Screw - M4x16',(#5676));
#5765=COLOUR_RGB('Black',0.12,0.14,0.17);
#5766=FILL_AREA_STYLE_COLOUR('',#5765);
#5767=FILL_AREA_STYLE('',(#5766));
#5768=SURFACE_STYLE_FILL_AREA(#5767);
#5769=SURFACE_SIDE_STYLE('',(#5768));
#5770=SURFACE_STYLE_USAGE(.BOTH.,#5769);
#5771=PRESENTATION_STYLE_ASSIGNMENT((#5770));
ENDSEC;
END-ISO-10303-21;
